ISO-10303-21;
HEADER;
FILE_DESCRIPTION (('STEP AP214'),
    '1' );
FILE_NAME ('socket head cap screw_iso_ISO 4762 M4 x 10 - 10N.step',
    '2026-10-08T13:22:57',
    ( '' ),
    ( '' ),
    'SwSTEP 2.0',
    'SolidWorks 2026',
    '' );
FILE_SCHEMA (( 'AUTOMOTIVE_DESIGN' ));
ENDSEC;

DATA;
#3=EDGE_CURVE ( 'NONE', #2841, #2214, #7627, .T. ) ;
#13=EDGE_CURVE ( 'NONE', #5655, #2841, #6772, .T. ) ;
#14=ORIENTED_EDGE ( 'NONE', *, *, #6088, .F. ) ;
#26=CARTESIAN_POINT ( 'NONE',  ( 2.000000000000001776, 0.000000000000000000, 0.000000000000000000 ) ) ;
#29=ORIENTED_EDGE ( 'NONE', *, *, #8994, .F. ) ;
#32=AXIS2_PLACEMENT_3D ( 'NONE', #6124, #2105, #1276 ) ;
#57=CARTESIAN_POINT ( 'NONE',  ( 0.000000000000000000, 1.773042676681366281, 0.000000000000000000 ) ) ;
#67=ADVANCED_BREP_SHAPE_REPRESENTATION ( '', ( #183, #3995 ), #2439 ) ;
#76=DIRECTION ( 'NONE',  ( 0.000000000000000000, 8.191099868251446680E-34, 1.000000000000000000 ) ) ;
#110=CIRCLE ( 'NONE', #5390, 0.2000000000000000944 ) ;
#117=CARTESIAN_POINT ( 'NONE',  ( 0.2000000000000057288, 4.041334437186265510E-16, -3.299999999999999822 ) ) ;
#129=CARTESIAN_POINT ( 'NONE',  ( 2.000000000000001776, 0.8865213383406900238, 1.535499999999967446 ) ) ;
#131=SURFACE_STYLE_FILL_AREA ( #8771 ) ;
#146=CARTESIAN_POINT ( 'NONE',  ( 0.000000000000000000, 0.8865213383407039016, -1.535500000000022958 ) ) ;
#161=EDGE_CURVE ( 'NONE', #3385, #4901, #5306, .T. ) ;
#167=LINE ( 'NONE', #8073, #9856 ) ;
#172=TOROIDAL_SURFACE ( 'NONE', #9093, 2.200000000000001066, 0.2000000000000000111 ) ;
#183=MANIFOLD_SOLID_BREP ( 'Hex', #8118 ) ;
#201=ORIENTED_EDGE ( 'NONE', *, *, #7622, .F. ) ;
#204=ORIENTED_EDGE ( 'NONE', *, *, #7487, .T. ) ;
#221=EDGE_LOOP ( 'NONE', ( #1092, #6507, #3813, #5099, #9566 ) ) ;
#233=ORIENTED_EDGE ( 'NONE', *, *, #6419, .T. ) ;
#245=CARTESIAN_POINT ( 'NONE',  ( 0.000000000000000000, 0.000000000000000000, 0.000000000000000000 ) ) ;
#269=CARTESIAN_POINT ( 'NONE',  ( 0.000000000000000000, 0.000000000000000000, 0.000000000000000000 ) ) ;
#296=ADVANCED_FACE ( 'NONE', ( #9134 ), #1342, .T. ) ;
#329=VECTOR ( 'NONE', #7005, 1000.000000000000000 ) ;
#364=ORIENTED_EDGE ( 'NONE', *, *, #6954, .T. ) ;
#384=CARTESIAN_POINT ( 'NONE',  ( 0.2000000000000057288, 2.703062956522977593E-33, 3.299999999999999822 ) ) ;
#405=LINE ( 'NONE', #3548, #2162 ) ;
#477=CARTESIAN_POINT ( 'NONE',  ( 2.000000000000001776, -0.8865213383406622683, -1.535500000000078469 ) ) ;
#508=AXIS2_PLACEMENT_3D ( 'NONE', #384, #7615, #536 ) ;
#514=CIRCLE ( 'NONE', #1996, 0.2000000000000000944 ) ;
#525=DIRECTION ( 'NONE',  ( 0.000000000000000000, 1.000000000000000000, -1.332267629550187849E-15 ) ) ;
#536=DIRECTION ( 'NONE',  ( 0.000000000000000000, -8.191099868251441548E-34, -1.000000000000000000 ) ) ;
#549=EDGE_CURVE ( 'NONE', #4723, #3726, #2398, .T. ) ;
#574=LINE ( 'NONE', #8420, #9956 ) ;
#579=CARTESIAN_POINT ( 'NONE',  ( 0.000000000000000000, 2.703062956522977593E-33, 3.299999999999999822 ) ) ;
#585=EDGE_CURVE ( 'NONE', #5107, #8149, #1491, .T. ) ;
#596=LINE ( 'NONE', #5391, #848 ) ;
#616=ADVANCED_FACE ( 'NONE', ( #854 ), #3309, .F. ) ;
#625=ORIENTED_EDGE ( 'NONE', *, *, #2876, .T. ) ;
#633=DIRECTION ( 'NONE',  ( 0.000000000000000000, -1.000000000000000000, 8.191099868251446680E-34 ) ) ;
#640=AXIS2_PLACEMENT_3D ( 'NONE', #8513, #4066, #1542 ) ;
#644=FACE_OUTER_BOUND ( 'NONE', #6077, .T. ) ;
#651=PLANE ( 'NONE',  #8473 ) ;
#666=FILL_AREA_STYLE ('',( #8623 ) ) ;
#687=AXIS2_PLACEMENT_3D ( 'NONE', #4950, #2617, #5245 ) ;
#690=EDGE_LOOP ( 'NONE', ( #3078, #6347, #4247, #9769 ) ) ;
#695=VECTOR ( 'NONE', #3899, 1000.000000000000000 ) ;
#706=CARTESIAN_POINT ( 'NONE',  ( 13.61000000000001720, 0.000000000000000000, 0.000000000000000000 ) ) ;
#716=EDGE_CURVE ( 'NONE', #2214, #4164, #4775, .T. ) ;
#737=TOROIDAL_SURFACE ( 'NONE', #6796, 3.299999999999999822, 0.2000000000000000111 ) ;
#743=FACE_OUTER_BOUND ( 'NONE', #221, .T. ) ;
#746=DIRECTION ( 'NONE',  ( 0.000000000000000000, -8.191099868251446680E-34, -1.000000000000000000 ) ) ;
#758=DIRECTION ( 'NONE',  ( 1.000000000000000000, -0.000000000000000000, -0.000000000000000000 ) ) ;
#760=FACE_OUTER_BOUND ( 'NONE', #4497, .T. ) ;
#765=PRESENTATION_STYLE_ASSIGNMENT (( #4690 ) ) ;
#782=AXIS2_PLACEMENT_3D ( 'NONE', #4977, #2444, #8966 ) ;
#797=CARTESIAN_POINT ( 'NONE',  ( 2.000000000000001776, 1.329782007511007169, 0.7677499999999559677 ) ) ;
#834=ORIENTED_EDGE ( 'NONE', *, *, #1944, .F. ) ;
#842=AXIS2_PLACEMENT_3D ( 'NONE', #8392, #10108, #4420 ) ;
#848=VECTOR ( 'NONE', #3742, 1000.000000000000114 ) ;
#853=DIRECTION ( 'NONE',  ( 0.000000000000000000, 8.191099868251446680E-34, 1.000000000000000000 ) ) ;
#854=FACE_OUTER_BOUND ( 'NONE', #1961, .T. ) ;
#887=DIRECTION ( 'NONE',  ( 0.000000000000000000, 8.191099868251448390E-34, 1.000000000000000000 ) ) ;
#899=DIRECTION ( 'NONE',  ( -1.000000000000000000, 0.000000000000000000, 0.000000000000000000 ) ) ;
#902=ORIENTED_EDGE ( 'NONE', *, *, #13, .F. ) ;
#915=CARTESIAN_POINT ( 'NONE',  ( 2.000000000000001776, -1.329782007510979636, 0.7677500000000114788 ) ) ;
#917=SURFACE_SIDE_STYLE ('',( #131 ) ) ;
#940=EDGE_LOOP ( 'NONE', ( #7377, #9310, #7961 ) ) ;
#952=FACE_OUTER_BOUND ( 'NONE', #9929, .T. ) ;
#958=CARTESIAN_POINT ( 'NONE',  ( 2.000000000000001776, -1.329782007510993402, -0.7677500000000114788 ) ) ;
#962=ORIENTED_EDGE ( 'NONE', *, *, #4366, .T. ) ;
#987=EDGE_CURVE ( 'NONE', #8978, #9666, #1661, .T. ) ;
#995=CARTESIAN_POINT ( 'NONE',  ( 2.000000000000001776, -0.8865213383406622683, -1.535500000000078469 ) ) ;
#999=VERTEX_POINT ( 'NONE', #1504 ) ;
#1012=VECTOR ( 'NONE', #2875, 1000.000000000000000 ) ;
#1032=ORIENTED_EDGE ( 'NONE', *, *, #9471, .F. ) ;
#1044=EDGE_LOOP ( 'NONE', ( #14, #3815, #5005, #1903, #4389 ) ) ;
#1091=ADVANCED_FACE ( 'NONE', ( #6123 ), #9299, .T. ) ;
#1092=ORIENTED_EDGE ( 'NONE', *, *, #549, .F. ) ;
#1112=DIRECTION ( 'NONE',  ( 1.000000000000000000, 0.000000000000000000, 0.000000000000000000 ) ) ;
#1114=VECTOR ( 'NONE', #4151, 1000.000000000000114 ) ;
#1116=ORIENTED_EDGE ( 'NONE', *, *, #9269, .T. ) ;
#1165=DIRECTION ( 'NONE',  ( -1.000000000000000000, -0.000000000000000000, -0.000000000000000000 ) ) ;
#1169=CONICAL_SURFACE ( 'NONE', #687, 1.610000000000000098, 0.7853981633974658205 ) ;
#1178=VERTEX_POINT ( 'NONE', #4737 ) ;
#1185=EDGE_CURVE ( 'NONE', #9817, #3385, #9399, .T. ) ;
#1213=LINE ( 'NONE', #6003, #3504 ) ;
#1219=UNCERTAINTY_MEASURE_WITH_UNIT (LENGTH_MEASURE( 1.000000000000000082E-05 ), #7838, 'distance_accuracy_value', 'NONE');
#1229=ORIENTED_EDGE ( 'NONE', *, *, #3196, .T. ) ;
#1237=VERTEX_POINT ( 'NONE', #6418 ) ;
#1243=PLANE ( 'NONE',  #8942 ) ;
#1255=EDGE_LOOP ( 'NONE', ( #9651, #4833 ) ) ;
#1276=DIRECTION ( 'NONE',  ( 0.000000000000000000, 8.191099868251448390E-34, 1.000000000000000000 ) ) ;
#1293=FACE_OUTER_BOUND ( 'NONE', #9168, .T. ) ;
#1294=LINE ( 'NONE', #4449, #2817 ) ;
#1296=ADVANCED_FACE ( 'NONE', ( #760 ), #1735, .T. ) ;
#1300=EDGE_CURVE ( 'NONE', #999, #2970, #2355, .T. ) ;
#1314=DIRECTION ( 'NONE',  ( -1.000000000000000000, 0.000000000000000000, 0.000000000000000000 ) ) ;
#1316=MECHANICAL_DESIGN_GEOMETRIC_PRESENTATION_REPRESENTATION('',(#5298),#9743);
#1332=VECTOR ( 'NONE', #3264, 1000.000000000000000 ) ;
#1342=TOROIDAL_SURFACE ( 'NONE', #9583, 3.299999999999999822, 0.2000000000000000111 ) ;
#1353=CARTESIAN_POINT ( 'NONE',  ( 4.200000000000009059, -1.802041971015319193E-33, -2.200000000000001066 ) ) ;
#1368=ORIENTED_EDGE ( 'NONE', *, *, #5122, .T. ) ;
#1401=CARTESIAN_POINT ( 'NONE',  ( 0.000000000000000000, -0.8865213383406622683, -1.535500000000078469 ) ) ;
#1427=PLANE ( 'NONE',  #6944 ) ;
#1459=CARTESIAN_POINT ( 'NONE',  ( 2.000000000000001776, -1.773042676681352292, -1.110223024625156540E-13 ) ) ;
#1461=( GEOMETRIC_REPRESENTATION_CONTEXT ( 3 ) GLOBAL_UNCERTAINTY_ASSIGNED_CONTEXT ( ( #1219 ) ) GLOBAL_UNIT_ASSIGNED_CONTEXT ( ( #7838, #3130, #5308 ) ) REPRESENTATION_CONTEXT ( 'NONE', 'WORKASPACE' ) );
#1478=DIRECTION ( 'NONE',  ( 1.000000000000000000, 0.000000000000000000, 0.000000000000000000 ) ) ;
#1489=SHAPE_REPRESENTATION_RELATIONSHIP ( 'NONE' , 'NONE' ,  #8171, #67 ) ;
#1491=CIRCLE ( 'NONE', #7429, 1.610000000000000098 ) ;
#1504=CARTESIAN_POINT ( 'NONE',  ( 13.61000000000001720, 2.449293598294708386E-16, -2.000000000000001332 ) ) ;
#1506=DIRECTION ( 'NONE',  ( -6.162975822039154730E-33, -0.4999999999999991118, 0.8660254037844391517 ) ) ;
#1509=CIRCLE ( 'NONE', #9927, 2.000000000000000888 ) ;
#1525=ORIENTED_EDGE ( 'NONE', *, *, #716, .T. ) ;
#1534=DIRECTION ( 'NONE',  ( -1.000000000000000000, 0.000000000000000000, 0.000000000000000000 ) ) ;
#1540=LINE ( 'NONE', #4687, #8260 ) ;
#1541=VERTEX_POINT ( 'NONE', #8047 ) ;
#1542=DIRECTION ( 'NONE',  ( 0.000000000000000000, -8.191099868251446680E-34, -1.000000000000000000 ) ) ;
#1544=( LENGTH_UNIT ( ) NAMED_UNIT ( * ) SI_UNIT ( .MILLI., .METRE. ) );
#1592=( NAMED_UNIT ( * ) PLANE_ANGLE_UNIT ( ) SI_UNIT ( $, .RADIAN. ) );
#1598=ADVANCED_FACE ( 'NONE', ( #9712 ), #1169, .T. ) ;
#1602=ORIENTED_EDGE ( 'NONE', *, *, #7750, .F. ) ;
#1604=LINE ( 'NONE', #3300, #3661 ) ;
#1620=LINE ( 'NONE', #4871, #1332 ) ;
#1622=EDGE_CURVE ( 'NONE', #5319, #5655, #405, .T. ) ;
#1628=CARTESIAN_POINT ( 'NONE',  ( 2.000000000000001776, 0.000000000000000000, 0.000000000000000000 ) ) ;
#1653=CARTESIAN_POINT ( 'NONE',  ( 4.200000000000009059, 0.000000000000000000, 0.000000000000000000 ) ) ;
#1661=CIRCLE ( 'NONE', #8917, 3.299999999999999822 ) ;
#1671=AXIS2_PLACEMENT_3D ( 'NONE', #6938, #5350, #8502 ) ;
#1672=AXIS2_PLACEMENT_3D ( 'NONE', #4974, #3942, #9683 ) ;
#1683=DIRECTION ( 'NONE',  ( -1.000000000000000000, 0.000000000000000000, 0.000000000000000000 ) ) ;
#1686=ADVANCED_FACE ( 'NONE', ( #2972 ), #9038, .T. ) ;
#1715=DIRECTION ( 'NONE',  ( 0.000000000000000000, -1.000000000000000000, 1.332267629550187849E-15 ) ) ;
#1729=FACE_OUTER_BOUND ( 'NONE', #8740, .T. ) ;
#1735=CYLINDRICAL_SURFACE ( 'NONE', #8585, 2.000000000000000888 ) ;
#1737=EDGE_LOOP ( 'NONE', ( #9620, #4128, #5037, #10200 ) ) ;
#1798=ORIENTED_EDGE ( 'NONE', *, *, #549, .T. ) ;
#1801=CARTESIAN_POINT ( 'NONE',  ( 2.000000000000001776, 0.8865213383407039016, -1.535500000000022958 ) ) ;
#1808=ORIENTED_EDGE ( 'NONE', *, *, #4409, .F. ) ;
#1820=DIRECTION ( 'NONE',  ( 0.000000000000000000, -1.224646799147353207E-16, 1.000000000000000000 ) ) ;
#1842=CONICAL_SURFACE ( 'NONE', #5792, 1.535500000000000087, 1.047197551196590748 ) ;
#1891=CARTESIAN_POINT ( 'NONE',  ( 2.000000000000001776, 1.329782007511007169, -0.7677500000000114788 ) ) ;
#1898=FACE_OUTER_BOUND ( 'NONE', #1044, .T. ) ;
#1903=ORIENTED_EDGE ( 'NONE', *, *, #3, .T. ) ;
#1930=DIRECTION ( 'NONE',  ( 0.000000000000000000, -8.191099868251446680E-34, -1.000000000000000000 ) ) ;
#1944=EDGE_CURVE ( 'NONE', #2935, #8072, #7779, .T. ) ;
#1949=CARTESIAN_POINT ( 'NONE',  ( 2.000000000000001776, -0.8865213383406761460, 1.535499999999911935 ) ) ;
#1961=EDGE_LOOP ( 'NONE', ( #9547, #8573, #8965, #2892, #5922 ) ) ;
#1966=FACE_OUTER_BOUND ( 'NONE', #9024, .T. ) ;
#1978=COLOUR_RGB ( '', 0.66274510, 0.83137255, 0.94901961) ;
#1983=VECTOR ( 'NONE', #3128, 1000.000000000000000 ) ;
#1993=CIRCLE ( 'NONE', #8594, 2.000000000000001332 ) ;
#1996=AXIS2_PLACEMENT_3D ( 'NONE', #9059, #4397, #4242 ) ;
#2036=DIRECTION ( 'NONE',  ( -1.000000000000000000, 0.000000000000000000, 0.000000000000000000 ) ) ;
#2052=ORIENTED_EDGE ( 'NONE', *, *, #161, .F. ) ;
#2070=PLANE ( 'NONE',  #7115 ) ;
#2088=CARTESIAN_POINT ( 'NONE',  ( 0.000000000000000000, -1.773042676681352292, -1.110223024625156540E-13 ) ) ;
#2096=EDGE_CURVE ( 'NONE', #2369, #4723, #1540, .T. ) ;
#2105=DIRECTION ( 'NONE',  ( -1.000000000000000000, 0.000000000000000000, 0.000000000000000000 ) ) ;
#2119=EDGE_CURVE ( 'NONE', #4139, #3726, #6269, .T. ) ;
#2154=CIRCLE ( 'NONE', #8096, 1.535500000000000087 ) ;
#2162=VECTOR ( 'NONE', #6837, 1000.000000000000000 ) ;
#2207=AXIS2_PLACEMENT_3D ( 'NONE', #8447, #1314, #9717 ) ;
#2212=VERTEX_POINT ( 'NONE', #915 ) ;
#2214=VERTEX_POINT ( 'NONE', #1891 ) ;
#2231=DIRECTION ( 'NONE',  ( 3.081487911019577365E-32, 0.4999999999999990008, -0.8660254037844391517 ) ) ;
#2235=CARTESIAN_POINT ( 'NONE',  ( 2.000000000000001776, -1.773042676681352292, -1.110223024625156540E-13 ) ) ;
#2271=ORIENTED_EDGE ( 'NONE', *, *, #6815, .F. ) ;
#2272=CYLINDRICAL_SURFACE ( 'NONE', #5880, 3.500000000000000000 ) ;
#2279=DIRECTION ( 'NONE',  ( 0.000000000000000000, -8.191099868251446680E-34, -1.000000000000000000 ) ) ;
#2300=CARTESIAN_POINT ( 'NONE',  ( 0.000000000000000000, 0.8865213383406900238, 1.535499999999967446 ) ) ;
#2319=ORIENTED_EDGE ( 'NONE', *, *, #8480, .F. ) ;
#2336=CARTESIAN_POINT ( 'NONE',  ( 0.2000000000000057288, 0.000000000000000000, 0.000000000000000000 ) ) ;
#2347=CARTESIAN_POINT ( 'NONE',  ( 14.00000000000000533, 1.971681346627238735E-16, -1.610000000000000098 ) ) ;
#2355=LINE ( 'NONE', #3229, #7258 ) ;
#2358=DIRECTION ( 'NONE',  ( 0.000000000000000000, -1.000000000000000000, 9.714451465470119729E-16 ) ) ;
#2369=VERTEX_POINT ( 'NONE', #7988 ) ;
#2371=EDGE_LOOP ( 'NONE', ( #962, #2319, #834 ) ) ;
#2379=DIRECTION ( 'NONE',  ( -0.7071067811865350272, 5.791982262216934087E-34, 0.7071067811865598962 ) ) ;
#2382=ORIENTED_EDGE ( 'NONE', *, *, #9479, .T. ) ;
#2389=EDGE_CURVE ( 'NONE', #1237, #4901, #9655, .T. ) ;
#2397=CARTESIAN_POINT ( 'NONE',  ( 14.00000000000000533, 1.318767078788482996E-33, 1.610000000000000098 ) ) ;
#2398=LINE ( 'NONE', #9388, #5266 ) ;
#2404=DIRECTION ( 'NONE',  ( -1.000000000000000000, 0.000000000000000000, 0.000000000000000000 ) ) ;
#2412=EDGE_CURVE ( 'NONE', #1541, #999, #1993, .T. ) ;
#2427=DIRECTION ( 'NONE',  ( -1.000000000000000000, 0.000000000000000000, 0.000000000000000000 ) ) ;
#2439=( GEOMETRIC_REPRESENTATION_CONTEXT ( 3 ) GLOBAL_UNCERTAINTY_ASSIGNED_CONTEXT ( ( #8673 ) ) GLOBAL_UNIT_ASSIGNED_CONTEXT ( ( #1544, #1592, #3966 ) ) REPRESENTATION_CONTEXT ( 'NONE', 'WORKASPACE' ) );
#2444=DIRECTION ( 'NONE',  ( 1.540743955509789230E-32, 0.8660254037844380415, -0.5000000000000012212 ) ) ;
#2475=CARTESIAN_POINT ( 'NONE',  ( 14.00000000000000533, 0.000000000000000000, 0.000000000000000000 ) ) ;
#2489=CARTESIAN_POINT ( 'NONE',  ( 0.000000000000000000, 4.163799117101000559E-16, -3.299999999999999822 ) ) ;
#2495=LINE ( 'NONE', #8021, #1114 ) ;
#2511=SURFACE_STYLE_USAGE ( .BOTH. , #917 ) ;
#2522=ORIENTED_EDGE ( 'NONE', *, *, #7750, .T. ) ;
#2594=TOROIDAL_SURFACE ( 'NONE', #8372, 2.200000000000001066, 0.2000000000000000111 ) ;
#2605=ORIENTED_EDGE ( 'NONE', *, *, #2801, .F. ) ;
#2617=DIRECTION ( 'NONE',  ( -1.000000000000000000, 0.000000000000000000, 0.000000000000000000 ) ) ;
#2635=DIRECTION ( 'NONE',  ( 0.000000000000000000, -9.714451465470119729E-16, -1.000000000000000000 ) ) ;
#2673=EDGE_LOOP ( 'NONE', ( #1525, #2522, #201 ) ) ;
#2720=EDGE_CURVE ( 'NONE', #8149, #999, #7043, .T. ) ;
#2791=DIRECTION ( 'NONE',  ( -1.000000000000000000, -0.000000000000000000, -0.000000000000000000 ) ) ;
#2801=EDGE_CURVE ( 'NONE', #3385, #4723, #596, .T. ) ;
#2817=VECTOR ( 'NONE', #1506, 1000.000000000000000 ) ;
#2824=ORIENTED_EDGE ( 'NONE', *, *, #4691, .T. ) ;
#2833=VERTEX_POINT ( 'NONE', #3947 ) ;
#2841=VERTEX_POINT ( 'NONE', #797 ) ;
#2875=DIRECTION ( 'NONE',  ( -6.162975822039154730E-33, -0.4999999999999991118, 0.8660254037844391517 ) ) ;
#2876=EDGE_CURVE ( 'NONE', #1178, #9145, #10152, .T. ) ;
#2890=DIRECTION ( 'NONE',  ( 0.000000000000000000, -8.191099868251446680E-34, -1.000000000000000000 ) ) ;
#2892=ORIENTED_EDGE ( 'NONE', *, *, #8368, .T. ) ;
#2909=LINE ( 'NONE', #3744, #9941 ) ;
#2935=VERTEX_POINT ( 'NONE', #10104 ) ;
#2938=DIRECTION ( 'NONE',  ( -1.000000000000000000, 0.000000000000000000, 0.000000000000000000 ) ) ;
#2957=ORIENTED_EDGE ( 'NONE', *, *, #4838, .T. ) ;
#2969=AXIS2_PLACEMENT_3D ( 'NONE', #6925, #6153, #746 ) ;
#2970=VERTEX_POINT ( 'NONE', #6107 ) ;
#2972=FACE_OUTER_BOUND ( 'NONE', #6686, .T. ) ;
#2979=SURFACE_SIDE_STYLE ('',( #3763 ) ) ;
#3002=ADVANCED_FACE ( 'NONE', ( #8499 ), #10202, .T. ) ;
#3016=DIRECTION ( 'NONE',  ( -1.000000000000000000, 0.000000000000000000, 0.000000000000000000 ) ) ;
#3017=DIRECTION ( 'NONE',  ( -1.000000000000000000, 0.000000000000000000, 0.000000000000000000 ) ) ;
#3031=VERTEX_POINT ( 'NONE', #3172 ) ;
#3065=CARTESIAN_POINT ( 'NONE',  ( -31.74999999999994316, 2.866884953888006423E-33, 3.500000000000000000 ) ) ;
#3068=DIRECTION ( 'NONE',  ( 0.000000000000000000, -8.191099868251446680E-34, -1.000000000000000000 ) ) ;
#3078=ORIENTED_EDGE ( 'NONE', *, *, #4094, .F. ) ;
#3112=DIRECTION ( 'NONE',  ( 3.081487911019577365E-32, 0.4999999999999990008, -0.8660254037844391517 ) ) ;
#3116=DIRECTION ( 'NONE',  ( -1.000000000000000000, 0.000000000000000000, 0.000000000000000000 ) ) ;
#3126=DIRECTION ( 'NONE',  ( -1.000000000000000000, 0.000000000000000000, 0.000000000000000000 ) ) ;
#3128=DIRECTION ( 'NONE',  ( -1.000000000000000000, 0.000000000000000000, 0.000000000000000000 ) ) ;
#3130=( NAMED_UNIT ( * ) PLANE_ANGLE_UNIT ( ) SI_UNIT ( $, .RADIAN. ) );
#3140=VECTOR ( 'NONE', #2358, 1000.000000000000000 ) ;
#3142=CIRCLE ( 'NONE', #8764, 3.500000000000000000 ) ;
#3167=AXIS2_PLACEMENT_3D ( 'NONE', #9300, #4381, #6841 ) ;
#3169=EDGE_LOOP ( 'NONE', ( #8751, #3311, #1032, #8588, #5554 ) ) ;
#3172=CARTESIAN_POINT ( 'NONE',  ( 0.000000000000000000, 1.773042676681366281, 0.000000000000000000 ) ) ;
#3175=FACE_OUTER_BOUND ( 'NONE', #2673, .T. ) ;
#3180=DIRECTION ( 'NONE',  ( 0.000000000000000000, 8.191099868251448390E-34, 1.000000000000000000 ) ) ;
#3196=EDGE_CURVE ( 'NONE', #3268, #8978, #110, .T. ) ;
#3203=DIRECTION ( 'NONE',  ( 0.000000000000000000, 8.191099868251446680E-34, 1.000000000000000000 ) ) ;
#3209=PLANE ( 'NONE',  #9602 ) ;
#3214=DIRECTION ( 'NONE',  ( -6.162975822039153635E-32, -0.5000000000000011102, -0.8660254037844379305 ) ) ;
#3222=CARTESIAN_POINT ( 'NONE',  ( 0.000000000000000000, -0.8865213383406761460, 1.535499999999911935 ) ) ;
#3229=CARTESIAN_POINT ( 'NONE',  ( -31.74999999999994316, 2.449293598294707893E-16, -2.000000000000000888 ) ) ;
#3236=ADVANCED_FACE ( 'NONE', ( #1729 ), #8906, .F. ) ;
#3264=DIRECTION ( 'NONE',  ( -1.000000000000000000, 0.000000000000000000, 0.000000000000000000 ) ) ;
#3268=VERTEX_POINT ( 'NONE', #9587 ) ;
#3298=EDGE_CURVE ( 'NONE', #2212, #2369, #2495, .T. ) ;
#3300=CARTESIAN_POINT ( 'NONE',  ( 2.000000000000001776, 0.8865213383407039016, -1.535500000000022958 ) ) ;
#3309=CONICAL_SURFACE ( 'NONE', #5611, 1.535500000000000087, 1.047197551196590748 ) ;
#3311=ORIENTED_EDGE ( 'NONE', *, *, #2389, .F. ) ;
#3314=DIRECTION ( 'NONE',  ( -1.000000000000000000, 0.000000000000000000, 0.000000000000000000 ) ) ;
#3340=EDGE_CURVE ( 'NONE', #2833, #3031, #167, .T. ) ;
#3356=FACE_OUTER_BOUND ( 'NONE', #1737, .T. ) ;
#3370=LINE ( 'NONE', #995, #6924 ) ;
#3385=VERTEX_POINT ( 'NONE', #3222 ) ;
#3408=ORIENTED_EDGE ( 'NONE', *, *, #9933, .T. ) ;
#3416=DIRECTION ( 'NONE',  ( 0.000000000000000000, 8.191099868251446680E-34, 1.000000000000000000 ) ) ;
#3425=FACE_OUTER_BOUND ( 'NONE', #690, .T. ) ;
#3431=DIRECTION ( 'NONE',  ( -1.000000000000000000, 0.000000000000000000, 0.000000000000000000 ) ) ;
#3441=ADVANCED_FACE ( 'NONE', ( #952 ), #6360, .T. ) ;
#3475=CIRCLE ( 'NONE', #9266, 3.500000000000000000 ) ;
#3504=VECTOR ( 'NONE', #6827, 1000.000000000000114 ) ;
#3513=ORIENTED_EDGE ( 'NONE', *, *, #4691, .F. ) ;
#3515=CIRCLE ( 'NONE', #8303, 2.200000000000001066 ) ;
#3521=CIRCLE ( 'NONE', #2207, 3.500000000000000000 ) ;
#3522=DIRECTION ( 'NONE',  ( -1.000000000000000000, 0.000000000000000000, 0.000000000000000000 ) ) ;
#3532=AXIS2_PLACEMENT_3D ( 'NONE', #6919, #3314, #5731 ) ;
#3548=CARTESIAN_POINT ( 'NONE',  ( 2.000000000000001776, 1.257743384770009870E-33, 1.535500000000000087 ) ) ;
#3556=SHAPE_DEFINITION_REPRESENTATION ( #6717, #8171 ) ;
#3558=ORIENTED_EDGE ( 'NONE', *, *, #4366, .F. ) ;
#3596=ORIENTED_EDGE ( 'NONE', *, *, #3340, .T. ) ;
#3607=ORIENTED_EDGE ( 'NONE', *, *, #6954, .F. ) ;
#3630=VECTOR ( 'NONE', #6257, 1000.000000000000114 ) ;
#3644=VECTOR ( 'NONE', #8007, 1000.000000000000000 ) ;
#3661=VECTOR ( 'NONE', #9518, 1000.000000000000000 ) ;
#3663=ORIENTED_EDGE ( 'NONE', *, *, #716, .F. ) ;
#3724=LINE ( 'NONE', #1459, #3819 ) ;
#3726=VERTEX_POINT ( 'NONE', #1401 ) ;
#3742=DIRECTION ( 'NONE',  ( -6.162975822039153635E-32, -0.5000000000000011102, -0.8660254037844379305 ) ) ;
#3744=CARTESIAN_POINT ( 'NONE',  ( -31.74999999999994316, 1.638219973650290020E-33, 2.000000000000000888 ) ) ;
#3746=DIRECTION ( 'NONE',  ( -6.162975822039153635E-32, -0.5000000000000011102, -0.8660254037844379305 ) ) ;
#3759=EDGE_LOOP ( 'NONE', ( #4277, #8497 ) ) ;
#3763=SURFACE_STYLE_FILL_AREA ( #666 ) ;
#3769=ADVANCED_FACE ( 'NONE', ( #7652 ), #2272, .T. ) ;
#3773=ORIENTED_EDGE ( 'NONE', *, *, #9018, .T. ) ;
#3788=DIRECTION ( 'NONE',  ( -0.5000000000000061062, 1.060575238724902601E-16, -0.8660254037844351549 ) ) ;
#3793=PLANE ( 'NONE',  #2969 ) ;
#3813=ORIENTED_EDGE ( 'NONE', *, *, #9711, .T. ) ;
#3815=ORIENTED_EDGE ( 'NONE', *, *, #1622, .T. ) ;
#3819=VECTOR ( 'NONE', #2231, 1000.000000000000227 ) ;
#3834=DIRECTION ( 'NONE',  ( 0.000000000000000000, 8.191099868251446680E-34, 1.000000000000000000 ) ) ;
#3889=DIRECTION ( 'NONE',  ( -2.465190328815661345E-32, -0.4999999999999987232, 0.8660254037844392627 ) ) ;
#3899=DIRECTION ( 'NONE',  ( -1.000000000000000000, 0.000000000000000000, 0.000000000000000000 ) ) ;
#3924=DIRECTION ( 'NONE',  ( 1.000000000000000000, 0.000000000000000000, 0.000000000000000000 ) ) ;
#3938=FACE_OUTER_BOUND ( 'NONE', #4483, .T. ) ;
#3942=DIRECTION ( 'NONE',  ( -1.000000000000000000, 0.000000000000000000, 0.000000000000000000 ) ) ;
#3947=CARTESIAN_POINT ( 'NONE',  ( 2.000000000000001776, 1.773042676681366281, 0.000000000000000000 ) ) ;
#3966=( NAMED_UNIT ( * ) SI_UNIT ( $, .STERADIAN. ) SOLID_ANGLE_UNIT ( ) );
#3978=ORIENTED_EDGE ( 'NONE', *, *, #8156, .F. ) ;
#3981=AXIS2_PLACEMENT_3D ( 'NONE', #1353, #633, #7600 ) ;
#3995=AXIS2_PLACEMENT_3D ( 'NONE', #245, #8930, #7419 ) ;
#4017=CARTESIAN_POINT ( 'NONE',  ( 2.000000000000001776, -0.8865213383406761460, 1.535499999999911935 ) ) ;
#4020=CIRCLE ( 'NONE', #9612, 2.000000000000001332 ) ;
#4033=ORIENTED_EDGE ( 'NONE', *, *, #6419, .F. ) ;
#4066=DIRECTION ( 'NONE',  ( 1.000000000000000000, 0.000000000000000000, 0.000000000000000000 ) ) ;
#4067=PRESENTATION_STYLE_ASSIGNMENT (( #2511 ) ) ;
#4083=CARTESIAN_POINT ( 'NONE',  ( 2.000000000000001776, -0.8865213383406761460, 1.535499999999911935 ) ) ;
#4094=EDGE_CURVE ( 'NONE', #8205, #2970, #4412, .T. ) ;
#4098=ADVANCED_FACE ( 'NONE', ( #3356 ), #2594, .F. ) ;
#4101=DIRECTION ( 'NONE',  ( 0.000000000000000000, 8.191099868251446680E-34, 1.000000000000000000 ) ) ;
#4128=ORIENTED_EDGE ( 'NONE', *, *, #9269, .F. ) ;
#4129=DIRECTION ( 'NONE',  ( -1.000000000000000000, 0.000000000000000000, 0.000000000000000000 ) ) ;
#4131=VECTOR ( 'NONE', #5500, 1000.000000000000114 ) ;
#4135=DIRECTION ( 'NONE',  ( -1.000000000000000000, 0.000000000000000000, 0.000000000000000000 ) ) ;
#4136=AXIS2_PLACEMENT_3D ( 'NONE', #7162, #8561, #9398 ) ;
#4139=VERTEX_POINT ( 'NONE', #146 ) ;
#4151=DIRECTION ( 'NONE',  ( -6.162975822039153635E-32, -0.5000000000000011102, -0.8660254037844379305 ) ) ;
#4164=VERTEX_POINT ( 'NONE', #1801 ) ;
#4174=AXIS2_PLACEMENT_3D ( 'NONE', #5322, #2938, #7808 ) ;
#4178=ORIENTED_EDGE ( 'NONE', *, *, #4094, .T. ) ;
#4186=EDGE_CURVE ( 'NONE', #6635, #1178, #7720, .T. ) ;
#4196=CARTESIAN_POINT ( 'NONE',  ( 4.200000000000009059, 0.000000000000000000, 0.000000000000000000 ) ) ;
#4240=AXIS2_PLACEMENT_3D ( 'NONE', #7680, #3116, #9438 ) ;
#4242=DIRECTION ( 'NONE',  ( 0.000000000000000000, 1.224646799147353207E-16, 1.000000000000000000 ) ) ;
#4247=ORIENTED_EDGE ( 'NONE', *, *, #7128, .F. ) ;
#4277=ORIENTED_EDGE ( 'NONE', *, *, #4838, .F. ) ;
#4303=CONICAL_SURFACE ( 'NONE', #6934, 1.610000000000000098, 0.7853981633974658205 ) ;
#4338=APPLICATION_CONTEXT ( 'automotive_design' ) ;
#4366=EDGE_CURVE ( 'NONE', #2935, #5915, #1604, .T. ) ;
#4381=DIRECTION ( 'NONE',  ( -1.000000000000000000, 0.000000000000000000, 0.000000000000000000 ) ) ;
#4385=PRODUCT_CONTEXT ( 'NONE', #4338, 'mechanical' ) ;
#4389=ORIENTED_EDGE ( 'NONE', *, *, #7622, .T. ) ;
#4397=DIRECTION ( 'NONE',  ( 0.000000000000000000, 1.000000000000000000, -1.224646799147353207E-16 ) ) ;
#4404=LINE ( 'NONE', #6040, #5659 ) ;
#4409=EDGE_CURVE ( 'NONE', #1541, #8205, #2909, .T. ) ;
#4412=CIRCLE ( 'NONE', #7052, 2.000000000000000888 ) ;
#4420=DIRECTION ( 'NONE',  ( 0.000000000000000000, 0.4999999999999991673, -0.8660254037844390407 ) ) ;
#4443=ORIENTED_EDGE ( 'NONE', *, *, #2412, .F. ) ;
#4449=CARTESIAN_POINT ( 'NONE',  ( 2.000000000000001776, 1.773042676681366281, 0.000000000000000000 ) ) ;
#4483=EDGE_LOOP ( 'NONE', ( #8536, #1229, #7197, #3978 ) ) ;
#4497=EDGE_LOOP ( 'NONE', ( #9724, #5205, #1116, #1808 ) ) ;
#4520=ORIENTED_EDGE ( 'NONE', *, *, #9479, .F. ) ;
#4578=LINE ( 'NONE', #8343, #4801 ) ;
#4581=DIRECTION ( 'NONE',  ( 0.000000000000000000, -1.000000000000000000, 9.714451465470119729E-16 ) ) ;
#4584=AXIS2_PLACEMENT_3D ( 'NONE', #6285, #4129, #3203 ) ;
#4591=EDGE_LOOP ( 'NONE', ( #2957, #3408, #5369, #7462 ) ) ;
#4609=DIRECTION ( 'NONE',  ( 1.000000000000000000, 0.000000000000000000, 0.000000000000000000 ) ) ;
#4652=ORIENTED_EDGE ( 'NONE', *, *, #6228, .F. ) ;
#4660=FACE_OUTER_BOUND ( 'NONE', #10025, .T. ) ;
#4664=DIRECTION ( 'NONE',  ( -1.000000000000000000, 0.000000000000000000, 0.000000000000000000 ) ) ;
#4687=CARTESIAN_POINT ( 'NONE',  ( 2.000000000000001776, -1.773042676681352292, -1.110223024625156540E-13 ) ) ;
#4690=SURFACE_STYLE_USAGE ( .BOTH. , #2979 ) ;
#4691=EDGE_CURVE ( 'NONE', #9817, #2212, #1213, .T. ) ;
#4700=ORIENTED_EDGE ( 'NONE', *, *, #5122, .F. ) ;
#4720=DIRECTION ( 'NONE',  ( -1.000000000000000000, 0.000000000000000000, 0.000000000000000000 ) ) ;
#4723=VERTEX_POINT ( 'NONE', #2088 ) ;
#4737=CARTESIAN_POINT ( 'NONE',  ( 4.000000000000003553, 2.866884953888006423E-33, 3.500000000000000000 ) ) ;
#4753=ORIENTED_EDGE ( 'NONE', *, *, #2720, .T. ) ;
#4775=LINE ( 'NONE', #5393, #4131 ) ;
#4801=VECTOR ( 'NONE', #3746, 1000.000000000000114 ) ;
#4811=ORIENTED_EDGE ( 'NONE', *, *, #987, .F. ) ;
#4826=DIRECTION ( 'NONE',  ( 0.000000000000000000, 8.191099868251446680E-34, 1.000000000000000000 ) ) ;
#4833=ORIENTED_EDGE ( 'NONE', *, *, #5587, .T. ) ;
#4838=EDGE_CURVE ( 'NONE', #1178, #6635, #3521, .T. ) ;
#4854=VECTOR ( 'NONE', #3214, 1000.000000000000114 ) ;
#4871=CARTESIAN_POINT ( 'NONE',  ( 2.000000000000001776, 0.8865213383407039016, -1.535500000000022958 ) ) ;
#4883=CARTESIAN_POINT ( 'NONE',  ( 4.200000000000009059, 0.000000000000000000, 0.000000000000000000 ) ) ;
#4901=VERTEX_POINT ( 'NONE', #2300 ) ;
#4927=PRODUCT_DEFINITION_FORMATION_WITH_SPECIFIED_SOURCE ( 'ANY', '', #9883, .NOT_KNOWN. ) ;
#4950=CARTESIAN_POINT ( 'NONE',  ( 14.00000000000000533, 0.000000000000000000, 0.000000000000000000 ) ) ;
#4974=CARTESIAN_POINT ( 'NONE',  ( 0.000000000000000000, 0.000000000000000000, 0.000000000000000000 ) ) ;
#4977=CARTESIAN_POINT ( 'NONE',  ( 2.000000000000001776, 1.773042676681366281, 0.000000000000000000 ) ) ;
#4993=CARTESIAN_POINT ( 'NONE',  ( 4.000000000000003553, 0.000000000000000000, 0.000000000000000000 ) ) ;
#5005=ORIENTED_EDGE ( 'NONE', *, *, #13, .T. ) ;
#5019=CARTESIAN_POINT ( 'NONE',  ( 0.2000000000000057288, 2.866884953888006423E-33, 3.500000000000000000 ) ) ;
#5021=ADVANCED_FACE ( 'NONE', ( #3175 ), #651, .F. ) ;
#5037=ORIENTED_EDGE ( 'NONE', *, *, #9692, .T. ) ;
#5047=DIRECTION ( 'NONE',  ( 0.000000000000000000, 8.191099868251448390E-34, 1.000000000000000000 ) ) ;
#5098=DIRECTION ( 'NONE',  ( 1.540743955509788409E-32, 0.8660254037844380415, -0.5000000000000012212 ) ) ;
#5099=ORIENTED_EDGE ( 'NONE', *, *, #8480, .T. ) ;
#5101=ORIENTED_EDGE ( 'NONE', *, *, #6228, .T. ) ;
#5107=VERTEX_POINT ( 'NONE', #2397 ) ;
#5122=EDGE_CURVE ( 'NONE', #999, #1541, #4020, .T. ) ;
#5132=ADVANCED_FACE ( 'NONE', ( #9492 ), #1427, .F. ) ;
#5205=ORIENTED_EDGE ( 'NONE', *, *, #1300, .T. ) ;
#5234=CARTESIAN_POINT ( 'NONE',  ( 13.61000000000001720, 0.000000000000000000, 0.000000000000000000 ) ) ;
#5238=PLANE ( 'NONE',  #1671 ) ;
#5245=DIRECTION ( 'NONE',  ( 0.000000000000000000, 8.191099868251446680E-34, 1.000000000000000000 ) ) ;
#5264=CARTESIAN_POINT ( 'NONE',  ( 2.000000000000001776, -0.8865213383406761460, 1.535499999999911935 ) ) ;
#5266=VECTOR ( 'NONE', #7785, 1000.000000000000227 ) ;
#5298=STYLED_ITEM ( 'NONE', ( #4067 ), #183 ) ;
#5306=LINE ( 'NONE', #8717, #329 ) ;
#5308=( NAMED_UNIT ( * ) SI_UNIT ( $, .STERADIAN. ) SOLID_ANGLE_UNIT ( ) );
#5319=VERTEX_POINT ( 'NONE', #8754 ) ;
#5322=CARTESIAN_POINT ( 'NONE',  ( 2.000000000000001776, 0.000000000000000000, 0.000000000000000000 ) ) ;
#5350=DIRECTION ( 'NONE',  ( 1.000000000000000000, 0.000000000000000000, 0.000000000000000000 ) ) ;
#5369=ORIENTED_EDGE ( 'NONE', *, *, #9792, .T. ) ;
#5377=CARTESIAN_POINT ( 'NONE',  ( 0.2000000000000057288, 0.000000000000000000, 0.000000000000000000 ) ) ;
#5390=AXIS2_PLACEMENT_3D ( 'NONE', #117, #7198, #1820 ) ;
#5391=CARTESIAN_POINT ( 'NONE',  ( 0.000000000000000000, -0.8865213383406761460, 1.535499999999911935 ) ) ;
#5393=CARTESIAN_POINT ( 'NONE',  ( 2.000000000000001776, 1.773042676681366281, 0.000000000000000000 ) ) ;
#5394=FACE_BOUND ( 'NONE', #1255, .T. ) ;
#5406=ORIENTED_EDGE ( 'NONE', *, *, #2720, .F. ) ;
#5419=DIRECTION ( 'NONE',  ( 0.000000000000000000, 8.191099868251446680E-34, 1.000000000000000000 ) ) ;
#5426=CARTESIAN_POINT ( 'NONE',  ( 2.000000000000001776, -0.8865213383406761460, 1.535499999999911935 ) ) ;
#5454=AXIS2_PLACEMENT_3D ( 'NONE', #9021, #1112, #1930 ) ;
#5458=( NAMED_UNIT ( * ) SI_UNIT ( $, .STERADIAN. ) SOLID_ANGLE_UNIT ( ) );
#5462=CIRCLE ( 'NONE', #3981, 0.2000000000000000944 ) ;
#5500=DIRECTION ( 'NONE',  ( -6.162975822039153635E-32, -0.5000000000000011102, -0.8660254037844379305 ) ) ;
#5503=DIRECTION ( 'NONE',  ( 0.000000000000000000, 8.191099868251446680E-34, 1.000000000000000000 ) ) ;
#5521=ORIENTED_EDGE ( 'NONE', *, *, #5747, .T. ) ;
#5529=FACE_OUTER_BOUND ( 'NONE', #3169, .T. ) ;
#5554=ORIENTED_EDGE ( 'NONE', *, *, #1185, .T. ) ;
#5577=ORIENTED_EDGE ( 'NONE', *, *, #3196, .F. ) ;
#5587=EDGE_CURVE ( 'NONE', #7530, #5864, #3515, .T. ) ;
#5590=DIRECTION ( 'NONE',  ( -1.000000000000000000, 0.000000000000000000, 0.000000000000000000 ) ) ;
#5611=AXIS2_PLACEMENT_3D ( 'NONE', #1628, #3017, #9338 ) ;
#5655=VERTEX_POINT ( 'NONE', #7454 ) ;
#5659=VECTOR ( 'NONE', #9066, 1000.000000000000000 ) ;
#5674=DIRECTION ( 'NONE',  ( 0.000000000000000000, -8.191099868251446680E-34, -1.000000000000000000 ) ) ;
#5691=ORIENTED_EDGE ( 'NONE', *, *, #1300, .F. ) ;
#5719=CARTESIAN_POINT ( 'NONE',  ( 4.200000000000009059, 0.000000000000000000, 0.000000000000000000 ) ) ;
#5731=DIRECTION ( 'NONE',  ( 0.000000000000000000, 8.191099868251446680E-34, 1.000000000000000000 ) ) ;
#5747=EDGE_CURVE ( 'NONE', #3031, #4901, #4404, .T. ) ;
#5759=CARTESIAN_POINT ( 'NONE',  ( 2.000000000000001776, 0.000000000000000000, 0.000000000000000000 ) ) ;
#5792=AXIS2_PLACEMENT_3D ( 'NONE', #5759, #5857, #5047 ) ;
#5857=DIRECTION ( 'NONE',  ( -1.000000000000000000, 0.000000000000000000, 0.000000000000000000 ) ) ;
#5864=VERTEX_POINT ( 'NONE', #9888 ) ;
#5880=AXIS2_PLACEMENT_3D ( 'NONE', #7754, #7019, #5419 ) ;
#5881=CARTESIAN_POINT ( 'NONE',  ( 2.000000000000001776, 0.8865213383407039016, -1.535500000000022958 ) ) ;
#5915=VERTEX_POINT ( 'NONE', #477 ) ;
#5922=ORIENTED_EDGE ( 'NONE', *, *, #6815, .T. ) ;
#5932=DIRECTION ( 'NONE',  ( 0.000000000000000000, 1.000000000000000000, -9.714451465470119729E-16 ) ) ;
#5939=DIRECTION ( 'NONE',  ( 0.000000000000000000, -8.191099868251446680E-34, -1.000000000000000000 ) ) ;
#5984=FACE_OUTER_BOUND ( 'NONE', #9322, .T. ) ;
#5996=FACE_OUTER_BOUND ( 'NONE', #7743, .T. ) ;
#6003=CARTESIAN_POINT ( 'NONE',  ( 2.000000000000001776, -0.8865213383406761460, 1.535499999999911935 ) ) ;
#6006=PLANE ( 'NONE',  #842 ) ;
#6040=CARTESIAN_POINT ( 'NONE',  ( 0.000000000000000000, 1.773042676681366281, 0.000000000000000000 ) ) ;
#6045=APPLICATION_CONTEXT ( 'automotive_design' ) ;
#6060=ADVANCED_FACE ( 'NONE', ( #743 ), #7862, .T. ) ;
#6077=EDGE_LOOP ( 'NONE', ( #6490, #3607, #902 ) ) ;
#6081=ADVANCED_FACE ( 'NONE', ( #3938 ), #737, .T. ) ;
#6086=DIRECTION ( 'NONE',  ( 1.000000000000000000, 0.000000000000000000, 0.000000000000000000 ) ) ;
#6088=EDGE_CURVE ( 'NONE', #5319, #2935, #9272, .T. ) ;
#6098=CIRCLE ( 'NONE', #508, 0.2000000000000000944 ) ;
#6104=AXIS2_PLACEMENT_3D ( 'NONE', #1949, #5098, #8248 ) ;
#6106=AXIS2_PLACEMENT_3D ( 'NONE', #26, #1534, #3180 ) ;
#6107=CARTESIAN_POINT ( 'NONE',  ( 4.200000000000009059, 2.449293598294707893E-16, -2.000000000000000888 ) ) ;
#6108=AXIS2_PLACEMENT_3D ( 'NONE', #9263, #6086, #2279 ) ;
#6111=CARTESIAN_POINT ( 'NONE',  ( 4.000000000000007105, 2.694222958124178486E-16, 2.200000000000001066 ) ) ;
#6114=CARTESIAN_POINT ( 'NONE',  ( 0.2000000000000057288, 0.000000000000000000, 0.000000000000000000 ) ) ;
#6123=FACE_OUTER_BOUND ( 'NONE', #9767, .T. ) ;
#6124=CARTESIAN_POINT ( 'NONE',  ( 2.000000000000001776, 0.000000000000000000, 0.000000000000000000 ) ) ;
#6142=PLANE ( 'NONE',  #6594 ) ;
#6153=DIRECTION ( 'NONE',  ( 1.000000000000000000, 0.000000000000000000, 0.000000000000000000 ) ) ;
#6160=AXIS2_PLACEMENT_3D ( 'NONE', #2235, #9325, #3889 ) ;
#6211=DIRECTION ( 'NONE',  ( 1.000000000000000000, 0.000000000000000000, 0.000000000000000000 ) ) ;
#6228=EDGE_CURVE ( 'NONE', #8149, #5107, #9473, .T. ) ;
#6241=DIRECTION ( 'NONE',  ( 1.000000000000000000, -0.000000000000000000, -0.000000000000000000 ) ) ;
#6257=DIRECTION ( 'NONE',  ( -0.7071067811865350272, 8.659560562355083235E-17, -0.7071067811865598962 ) ) ;
#6269=LINE ( 'NONE', #9453, #3140 ) ;
#6284=ORIENTED_EDGE ( 'NONE', *, *, #4186, .T. ) ;
#6285=CARTESIAN_POINT ( 'NONE',  ( 4.000000000000003553, 0.000000000000000000, 0.000000000000000000 ) ) ;
#6347=ORIENTED_EDGE ( 'NONE', *, *, #9121, .T. ) ;
#6360=CYLINDRICAL_SURFACE ( 'NONE', #9203, 2.000000000000000888 ) ;
#6394=DIRECTION ( 'NONE',  ( 6.162975822039154730E-32, 1.332267629550187849E-15, 1.000000000000000000 ) ) ;
#6397=ORIENTED_EDGE ( 'NONE', *, *, #8994, .T. ) ;
#6409=ORIENTED_EDGE ( 'NONE', *, *, #585, .T. ) ;
#6418=CARTESIAN_POINT ( 'NONE',  ( 2.000000000000001776, 0.8865213383406900238, 1.535499999999967446 ) ) ;
#6419=EDGE_CURVE ( 'NONE', #3031, #4139, #7341, .T. ) ;
#6448=DIRECTION ( 'NONE',  ( 0.000000000000000000, 8.191099868251446680E-34, 1.000000000000000000 ) ) ;
#6450=ORIENTED_EDGE ( 'NONE', *, *, #2096, .T. ) ;
#6490=ORIENTED_EDGE ( 'NONE', *, *, #9471, .T. ) ;
#6507=ORIENTED_EDGE ( 'NONE', *, *, #2096, .F. ) ;
#6534=ORIENTED_EDGE ( 'NONE', *, *, #2801, .T. ) ;
#6588=CIRCLE ( 'NONE', #1672, 3.299999999999999822 ) ;
#6593=CIRCLE ( 'NONE', #6106, 1.535500000000000087 ) ;
#6594=AXIS2_PLACEMENT_3D ( 'NONE', #10134, #4609, #2890 ) ;
#6616=ORIENTED_EDGE ( 'NONE', *, *, #9933, .F. ) ;
#6635=VERTEX_POINT ( 'NONE', #9828 ) ;
#6664=ORIENTED_EDGE ( 'NONE', *, *, #7657, .F. ) ;
#6666=DIRECTION ( 'NONE',  ( 0.000000000000000000, 8.191099868251446680E-34, 1.000000000000000000 ) ) ;
#6670=UNCERTAINTY_MEASURE_WITH_UNIT (LENGTH_MEASURE( 1.000000000000000082E-05 ), #7797, 'distance_accuracy_value', 'NONE');
#6686=EDGE_LOOP ( 'NONE', ( #2605, #6728, #2824, #7805, #6450 ) ) ;
#6689=ORIENTED_EDGE ( 'NONE', *, *, #7657, .T. ) ;
#6717=PRODUCT_DEFINITION_SHAPE ( 'NONE', 'NONE',  #9288 ) ;
#6728=ORIENTED_EDGE ( 'NONE', *, *, #1185, .F. ) ;
#6767=DIRECTION ( 'NONE',  ( -1.000000000000000000, 0.000000000000000000, 0.000000000000000000 ) ) ;
#6772=CIRCLE ( 'NONE', #3167, 1.535500000000000087 ) ;
#6796=AXIS2_PLACEMENT_3D ( 'NONE', #2336, #4664, #7033 ) ;
#6815=EDGE_CURVE ( 'NONE', #2212, #5655, #8637, .T. ) ;
#6827=DIRECTION ( 'NONE',  ( -6.162975822039153635E-32, -0.5000000000000011102, -0.8660254037844379305 ) ) ;
#6836=EDGE_CURVE ( 'NONE', #9817, #5655, #574, .T. ) ;
#6837=DIRECTION ( 'NONE',  ( -0.5000000000000061062, 7.093700570841092585E-34, 0.8660254037844351549 ) ) ;
#6841=DIRECTION ( 'NONE',  ( 0.000000000000000000, 8.191099868251448390E-34, 1.000000000000000000 ) ) ;
#6866=CARTESIAN_POINT ( 'NONE',  ( 2.000000000000001776, 1.880445160090761061E-16, -1.535500000000000087 ) ) ;
#6871=CARTESIAN_POINT ( 'NONE',  ( 2.000000000000001776, -1.773042676681352292, -1.110223024625156540E-13 ) ) ;
#6919=CARTESIAN_POINT ( 'NONE',  ( 14.00000000000000533, 0.000000000000000000, 0.000000000000000000 ) ) ;
#6924=VECTOR ( 'NONE', #899, 1000.000000000000000 ) ;
#6925=CARTESIAN_POINT ( 'NONE',  ( 2.000000000000001776, 1.773042676681366281, 0.000000000000000000 ) ) ;
#6934=AXIS2_PLACEMENT_3D ( 'NONE', #2475, #4135, #6448 ) ;
#6936=CARTESIAN_POINT ( 'NONE',  ( 2.000000000000001776, 1.773042676681366281, 0.000000000000000000 ) ) ;
#6937=CARTESIAN_POINT ( 'NONE',  ( 0.2000000000000057288, 0.000000000000000000, 0.000000000000000000 ) ) ;
#6938=CARTESIAN_POINT ( 'NONE',  ( 4.000000000000003553, 3.500000000000003109, 0.000000000000000000 ) ) ;
#6944=AXIS2_PLACEMENT_3D ( 'NONE', #10204, #1478, #3068 ) ;
#6954=EDGE_CURVE ( 'NONE', #2841, #1237, #9350, .T. ) ;
#6962=EDGE_LOOP ( 'NONE', ( #5577, #6664, #9777, #4811 ) ) ;
#7005=DIRECTION ( 'NONE',  ( 0.000000000000000000, 1.000000000000000000, -1.332267629550187849E-15 ) ) ;
#7019=DIRECTION ( 'NONE',  ( -1.000000000000000000, 0.000000000000000000, 0.000000000000000000 ) ) ;
#7033=DIRECTION ( 'NONE',  ( 0.000000000000000000, 8.191099868251446680E-34, 1.000000000000000000 ) ) ;
#7043=LINE ( 'NONE', #2347, #3630 ) ;
#7052=AXIS2_PLACEMENT_3D ( 'NONE', #1653, #3924, #5674 ) ;
#7067=DIRECTION ( 'NONE',  ( 0.000000000000000000, -8.191099868251446680E-34, -1.000000000000000000 ) ) ;
#7115=AXIS2_PLACEMENT_3D ( 'NONE', #269, #3522, #3416 ) ;
#7128=EDGE_CURVE ( 'NONE', #5864, #7530, #8261, .T. ) ;
#7135=CARTESIAN_POINT ( 'NONE',  ( -31.74999999999994316, 4.286263797015736595E-16, -3.500000000000000000 ) ) ;
#7156=CARTESIAN_POINT ( 'NONE',  ( 14.00000000000000533, 2.210487472460973684E-16, -1.610000000000000098 ) ) ;
#7158=CARTESIAN_POINT ( 'NONE',  ( -31.74999999999994316, 0.000000000000000000, 0.000000000000000000 ) ) ;
#7162=CARTESIAN_POINT ( 'NONE',  ( 2.000000000000001776, 0.000000000000000000, 0.000000000000000000 ) ) ;
#7177=ORIENTED_EDGE ( 'NONE', *, *, #987, .T. ) ;
#7186=ORIENTED_EDGE ( 'NONE', *, *, #7487, .F. ) ;
#7197=ORIENTED_EDGE ( 'NONE', *, *, #9018, .F. ) ;
#7198=DIRECTION ( 'NONE',  ( 0.000000000000000000, 1.000000000000000000, 1.224646799147353207E-16 ) ) ;
#7206=DIRECTION ( 'NONE',  ( -1.000000000000000000, 0.000000000000000000, 0.000000000000000000 ) ) ;
#7209=ORIENTED_EDGE ( 'NONE', *, *, #585, .F. ) ;
#7258=VECTOR ( 'NONE', #7206, 1000.000000000000000 ) ;
#7337=ADVANCED_FACE ( 'NONE', ( #5394, #9957 ), #5238, .T. ) ;
#7341=LINE ( 'NONE', #57, #4854 ) ;
#7345=DIRECTION ( 'NONE',  ( 0.000000000000000000, -8.191099868251446680E-34, -1.000000000000000000 ) ) ;
#7357=DIRECTION ( 'NONE',  ( 0.000000000000000000, -8.191099868251446680E-34, -1.000000000000000000 ) ) ;
#7377=ORIENTED_EDGE ( 'NONE', *, *, #9711, .F. ) ;
#7419=DIRECTION ( 'NONE',  ( 1.000000000000000000, 0.000000000000000000, 0.000000000000000000 ) ) ;
#7423=ADVANCED_FACE ( 'NONE', ( #9229 ), #6006, .T. ) ;
#7429=AXIS2_PLACEMENT_3D ( 'NONE', #8755, #1683, #4826 ) ;
#7430=VECTOR ( 'NONE', #3112, 1000.000000000000227 ) ;
#7454=CARTESIAN_POINT ( 'NONE',  ( 2.000000000000001776, 2.775557561562891351E-14, 1.535499999999967446 ) ) ;
#7457=CARTESIAN_POINT ( 'NONE',  ( 4.200000000000009059, 1.638219973650290020E-33, 2.000000000000000888 ) ) ;
#7462=ORIENTED_EDGE ( 'NONE', *, *, #2876, .F. ) ;
#7487=EDGE_CURVE ( 'NONE', #2833, #2214, #4578, .T. ) ;
#7517=DIRECTION ( 'NONE',  ( -1.000000000000000000, 0.000000000000000000, 0.000000000000000000 ) ) ;
#7530=VERTEX_POINT ( 'NONE', #6111 ) ;
#7600=DIRECTION ( 'NONE',  ( 0.000000000000000000, -8.191099868251441548E-34, -1.000000000000000000 ) ) ;
#7615=DIRECTION ( 'NONE',  ( 0.000000000000000000, -1.000000000000000000, 8.191099868251446680E-34 ) ) ;
#7622=EDGE_CURVE ( 'NONE', #2214, #2935, #6593, .T. ) ;
#7627=CIRCLE ( 'NONE', #32, 1.535500000000000087 ) ;
#7652=FACE_OUTER_BOUND ( 'NONE', #4591, .T. ) ;
#7657=EDGE_CURVE ( 'NONE', #9145, #3268, #3142, .T. ) ;
#7680=CARTESIAN_POINT ( 'NONE',  ( -31.74999999999994316, 0.000000000000000000, 0.000000000000000000 ) ) ;
#7712=LINE ( 'NONE', #5264, #9439 ) ;
#7720=CIRCLE ( 'NONE', #4584, 3.500000000000000000 ) ;
#7732=STYLED_ITEM ( 'NONE', ( #765 ), #67 ) ;
#7743=EDGE_LOOP ( 'NONE', ( #3513, #8357, #2271 ) ) ;
#7750=EDGE_CURVE ( 'NONE', #4164, #2935, #9391, .T. ) ;
#7754=CARTESIAN_POINT ( 'NONE',  ( -31.74999999999994316, 0.000000000000000000, 0.000000000000000000 ) ) ;
#7779=CIRCLE ( 'NONE', #4136, 1.535500000000000087 ) ;
#7785=DIRECTION ( 'NONE',  ( 3.081487911019577365E-32, 0.4999999999999990008, -0.8660254037844391517 ) ) ;
#7797=( LENGTH_UNIT ( ) NAMED_UNIT ( * ) SI_UNIT ( .MILLI., .METRE. ) );
#7805=ORIENTED_EDGE ( 'NONE', *, *, #3298, .T. ) ;
#7808=DIRECTION ( 'NONE',  ( 0.000000000000000000, 8.191099868251448390E-34, 1.000000000000000000 ) ) ;
#7827=DIRECTION ( 'NONE',  ( 0.000000000000000000, -8.191099868251446680E-34, -1.000000000000000000 ) ) ;
#7836=( NAMED_UNIT ( * ) PLANE_ANGLE_UNIT ( ) SI_UNIT ( $, .RADIAN. ) );
#7838=( LENGTH_UNIT ( ) NAMED_UNIT ( * ) SI_UNIT ( .MILLI., .METRE. ) );
#7862=PLANE ( 'NONE',  #6160 ) ;
#7918=ORIENTED_EDGE ( 'NONE', *, *, #4409, .T. ) ;
#7933=ORIENTED_EDGE ( 'NONE', *, *, #10033, .F. ) ;
#7959=CARTESIAN_POINT ( 'NONE',  ( 14.00000000000000533, 1.318767078788482996E-33, 1.610000000000000098 ) ) ;
#7961=ORIENTED_EDGE ( 'NONE', *, *, #8368, .F. ) ;
#7988=CARTESIAN_POINT ( 'NONE',  ( 2.000000000000001776, -1.773042676681352292, -1.110223024625156540E-13 ) ) ;
#7990=FILL_AREA_STYLE_COLOUR ( '', #1978 ) ;
#8007=DIRECTION ( 'NONE',  ( -1.000000000000000000, 0.000000000000000000, 0.000000000000000000 ) ) ;
#8021=CARTESIAN_POINT ( 'NONE',  ( 2.000000000000001776, -0.8865213383406761460, 1.535499999999911935 ) ) ;
#8028=DIRECTION ( 'NONE',  ( 1.000000000000000000, 0.000000000000000000, 0.000000000000000000 ) ) ;
#8047=CARTESIAN_POINT ( 'NONE',  ( 13.61000000000001720, 1.638219973650290362E-33, 2.000000000000001332 ) ) ;
#8070=ADVANCED_FACE ( 'NONE', ( #3425 ), #172, .F. ) ;
#8072=VERTEX_POINT ( 'NONE', #958 ) ;
#8073=CARTESIAN_POINT ( 'NONE',  ( 2.000000000000001776, 1.773042676681366281, 0.000000000000000000 ) ) ;
#8096=AXIS2_PLACEMENT_3D ( 'NONE', #9329, #4720, #10197 ) ;
#8118=CLOSED_SHELL ( 'NONE', ( #616, #6081, #8070, #1598, #1296, #3769, #9335, #3002, #7337, #3441, #9909, #1091, #4098, #296, #7423, #10055, #1686, #6060, #9142, #3236, #9723, #5132, #8181, #8583, #9505, #5021, #10223 ) ) ;
#8149=VERTEX_POINT ( 'NONE', #7156 ) ;
#8151=EDGE_LOOP ( 'NONE', ( #8512, #8169, #2382, #364, #9196 ) ) ;
#8156=EDGE_CURVE ( 'NONE', #9145, #9666, #6098, .T. ) ;
#8169=ORIENTED_EDGE ( 'NONE', *, *, #3340, .F. ) ;
#8171=SHAPE_REPRESENTATION ( 'socket head cap screw_iso_ISO 4762 M4 x 10 - 10N', ( #3995 ), #2439 ) ;
#8181=ADVANCED_FACE ( 'NONE', ( #5996 ), #9175, .F. ) ;
#8205=VERTEX_POINT ( 'NONE', #7457 ) ;
#8207=COLOUR_RGB ( '', 0.66274510, 0.83137255, 0.94901961) ;
#8248=DIRECTION ( 'NONE',  ( 6.162975822039153635E-32, 0.5000000000000011102, 0.8660254037844379305 ) ) ;
#8260=VECTOR ( 'NONE', #3126, 1000.000000000000000 ) ;
#8261=CIRCLE ( 'NONE', #9760, 2.200000000000001066 ) ;
#8262=VECTOR ( 'NONE', #2379, 1000.000000000000114 ) ;
#8303=AXIS2_PLACEMENT_3D ( 'NONE', #9990, #2791, #5939 ) ;
#8325=DIRECTION ( 'NONE',  ( 1.000000000000000000, 0.000000000000000000, 0.000000000000000000 ) ) ;
#8343=CARTESIAN_POINT ( 'NONE',  ( 2.000000000000001776, 1.773042676681366281, 0.000000000000000000 ) ) ;
#8357=ORIENTED_EDGE ( 'NONE', *, *, #6836, .T. ) ;
#8368=EDGE_CURVE ( 'NONE', #8072, #2212, #2154, .T. ) ;
#8372=AXIS2_PLACEMENT_3D ( 'NONE', #5719, #8733, #7067 ) ;
#8392=CARTESIAN_POINT ( 'NONE',  ( 2.000000000000001776, 1.773042676681366281, 0.000000000000000000 ) ) ;
#8420=CARTESIAN_POINT ( 'NONE',  ( 2.000000000000001776, -0.8865213383406761460, 1.535499999999911935 ) ) ;
#8447=CARTESIAN_POINT ( 'NONE',  ( 4.000000000000003553, 0.000000000000000000, 0.000000000000000000 ) ) ;
#8473=AXIS2_PLACEMENT_3D ( 'NONE', #6936, #6211, #7827 ) ;
#8478=DIRECTION ( 'NONE',  ( 0.000000000000000000, 1.000000000000000000, -1.332267629550187849E-15 ) ) ;
#8480=EDGE_CURVE ( 'NONE', #8072, #5915, #8596, .T. ) ;
#8484=FACE_OUTER_BOUND ( 'NONE', #2371, .T. ) ;
#8486=EDGE_LOOP ( 'NONE', ( #6616, #6284, #625, #6689 ) ) ;
#8497=ORIENTED_EDGE ( 'NONE', *, *, #4186, .F. ) ;
#8499=FACE_OUTER_BOUND ( 'NONE', #8486, .T. ) ;
#8502=DIRECTION ( 'NONE',  ( 0.000000000000000000, -8.191099868251446680E-34, -1.000000000000000000 ) ) ;
#8512=ORIENTED_EDGE ( 'NONE', *, *, #5747, .F. ) ;
#8513=CARTESIAN_POINT ( 'NONE',  ( 14.00000000000000533, 1.609999999999986553, 5.551115123125782702E-14 ) ) ;
#8533=PLANE ( 'NONE',  #6108 ) ;
#8536=ORIENTED_EDGE ( 'NONE', *, *, #9792, .F. ) ;
#8561=DIRECTION ( 'NONE',  ( -1.000000000000000000, 0.000000000000000000, 0.000000000000000000 ) ) ;
#8573=ORIENTED_EDGE ( 'NONE', *, *, #6088, .T. ) ;
#8583=ADVANCED_FACE ( 'NONE', ( #644 ), #3793, .F. ) ;
#8585=AXIS2_PLACEMENT_3D ( 'NONE', #7158, #2404, #76 ) ;
#8588=ORIENTED_EDGE ( 'NONE', *, *, #6836, .F. ) ;
#8594=AXIS2_PLACEMENT_3D ( 'NONE', #5234, #6767, #6666 ) ;
#8596=LINE ( 'NONE', #6871, #7430 ) ;
#8623=FILL_AREA_STYLE_COLOUR ( '', #8207 ) ;
#8637=CIRCLE ( 'NONE', #4174, 1.535500000000000087 ) ;
#8654=ORIENTED_EDGE ( 'NONE', *, *, #2119, .F. ) ;
#8658=VECTOR ( 'NONE', #3788, 1000.000000000000000 ) ;
#8673=UNCERTAINTY_MEASURE_WITH_UNIT (LENGTH_MEASURE( 1.000000000000000082E-05 ), #1544, 'distance_accuracy_value', 'NONE');
#8717=CARTESIAN_POINT ( 'NONE',  ( 0.000000000000000000, -0.8865213383406761460, 1.535499999999911935 ) ) ;
#8733=DIRECTION ( 'NONE',  ( 1.000000000000000000, 0.000000000000000000, 0.000000000000000000 ) ) ;
#8740=EDGE_LOOP ( 'NONE', ( #233, #29, #3663, #7186, #3596 ) ) ;
#8751=ORIENTED_EDGE ( 'NONE', *, *, #161, .T. ) ;
#8754=CARTESIAN_POINT ( 'NONE',  ( 2.886521338340691578, 0.000000000000000000, 0.000000000000000000 ) ) ;
#8755=CARTESIAN_POINT ( 'NONE',  ( 14.00000000000000533, 0.000000000000000000, 0.000000000000000000 ) ) ;
#8763=VECTOR ( 'NONE', #3431, 1000.000000000000000 ) ;
#8764=AXIS2_PLACEMENT_3D ( 'NONE', #6114, #758, #5503 ) ;
#8771=FILL_AREA_STYLE ('',( #7990 ) ) ;
#8813=ORIENTED_EDGE ( 'NONE', *, *, #3, .F. ) ;
#8814=DIRECTION ( 'NONE',  ( -1.000000000000000000, 0.000000000000000000, 0.000000000000000000 ) ) ;
#8906=PLANE ( 'NONE',  #782 ) ;
#8917=AXIS2_PLACEMENT_3D ( 'NONE', #10183, #2427, #887 ) ;
#8928=VECTOR ( 'NONE', #4581, 1000.000000000000000 ) ;
#8930=DIRECTION ( 'NONE',  ( 0.000000000000000000, 0.000000000000000000, 1.000000000000000000 ) ) ;
#8942=AXIS2_PLACEMENT_3D ( 'NONE', #5881, #2635, #5932 ) ;
#8953=EDGE_CURVE ( 'NONE', #5915, #3726, #3370, .T. ) ;
#8965=ORIENTED_EDGE ( 'NONE', *, *, #1944, .T. ) ;
#8966=DIRECTION ( 'NONE',  ( 6.162975822039153635E-32, 0.5000000000000011102, 0.8660254037844379305 ) ) ;
#8978=VERTEX_POINT ( 'NONE', #2489 ) ;
#8994=EDGE_CURVE ( 'NONE', #4164, #4139, #1620, .T. ) ;
#9018=EDGE_CURVE ( 'NONE', #9666, #8978, #6588, .T. ) ;
#9021=CARTESIAN_POINT ( 'NONE',  ( 2.000000000000001776, 1.773042676681366281, 0.000000000000000000 ) ) ;
#9024=EDGE_LOOP ( 'NONE', ( #3773, #7177 ) ) ;
#9038=PLANE ( 'NONE',  #6104 ) ;
#9050=MECHANICAL_DESIGN_GEOMETRIC_PRESENTATION_REPRESENTATION('',(#7732),#1461);
#9059=CARTESIAN_POINT ( 'NONE',  ( 4.200000000000009059, 2.694222958124178486E-16, 2.200000000000001066 ) ) ;
#9066=DIRECTION ( 'NONE',  ( -6.162975822039154730E-33, -0.4999999999999991118, 0.8660254037844391517 ) ) ;
#9093=AXIS2_PLACEMENT_3D ( 'NONE', #4883, #8028, #7357 ) ;
#9121=EDGE_CURVE ( 'NONE', #8205, #7530, #514, .T. ) ;
#9134=FACE_OUTER_BOUND ( 'NONE', #6962, .T. ) ;
#9142=ADVANCED_FACE ( 'NONE', ( #5984 ), #1243, .F. ) ;
#9145=VERTEX_POINT ( 'NONE', #5019 ) ;
#9163=FACE_BOUND ( 'NONE', #9332, .T. ) ;
#9168=EDGE_LOOP ( 'NONE', ( #5406, #5101, #9676, #4700 ) ) ;
#9175=PLANE ( 'NONE',  #5454 ) ;
#9196=ORIENTED_EDGE ( 'NONE', *, *, #2389, .T. ) ;
#9203=AXIS2_PLACEMENT_3D ( 'NONE', #9537, #5590, #4101 ) ;
#9223=ORIENTED_EDGE ( 'NONE', *, *, #2119, .T. ) ;
#9228=DIRECTION ( 'NONE',  ( 0.000000000000000000, 8.191099868251446680E-34, 1.000000000000000000 ) ) ;
#9229=FACE_OUTER_BOUND ( 'NONE', #8151, .T. ) ;
#9263=CARTESIAN_POINT ( 'NONE',  ( 2.000000000000001776, 1.773042676681366281, 0.000000000000000000 ) ) ;
#9266=AXIS2_PLACEMENT_3D ( 'NONE', #5377, #6241, #3834 ) ;
#9269=EDGE_CURVE ( 'NONE', #2970, #8205, #1509, .T. ) ;
#9272=LINE ( 'NONE', #6866, #8658 ) ;
#9288=PRODUCT_DEFINITION ( 'UNKNOWN', '', #4927, #9809 ) ;
#9292=CARTESIAN_POINT ( 'NONE',  ( 2.000000000000001776, 0.8865213383407039016, -1.535500000000022958 ) ) ;
#9299=PLANE ( 'NONE',  #640 ) ;
#9300=CARTESIAN_POINT ( 'NONE',  ( 2.000000000000001776, 0.000000000000000000, 0.000000000000000000 ) ) ;
#9310=ORIENTED_EDGE ( 'NONE', *, *, #3298, .F. ) ;
#9322=EDGE_LOOP ( 'NONE', ( #9223, #9515, #3558, #1602, #6397 ) ) ;
#9325=DIRECTION ( 'NONE',  ( -6.162975822039151993E-33, 0.8660254037844393737, 0.4999999999999987788 ) ) ;
#9329=CARTESIAN_POINT ( 'NONE',  ( 2.000000000000001776, 0.000000000000000000, 0.000000000000000000 ) ) ;
#9332=EDGE_LOOP ( 'NONE', ( #5521, #2052, #6534, #1798, #8654, #4033 ) ) ;
#9335=ADVANCED_FACE ( 'NONE', ( #9163, #1966 ), #2070, .T. ) ;
#9338=DIRECTION ( 'NONE',  ( 0.000000000000000000, 8.191099868251448390E-34, 1.000000000000000000 ) ) ;
#9350=LINE ( 'NONE', #9968, #1012 ) ;
#9388=CARTESIAN_POINT ( 'NONE',  ( 0.000000000000000000, -1.773042676681352292, -1.110223024625156540E-13 ) ) ;
#9391=LINE ( 'NONE', #9292, #8928 ) ;
#9398=DIRECTION ( 'NONE',  ( 0.000000000000000000, 8.191099868251448390E-34, 1.000000000000000000 ) ) ;
#9399=LINE ( 'NONE', #4017, #1983 ) ;
#9438=DIRECTION ( 'NONE',  ( 0.000000000000000000, 8.191099868251446680E-34, 1.000000000000000000 ) ) ;
#9439=VECTOR ( 'NONE', #525, 1000.000000000000000 ) ;
#9453=CARTESIAN_POINT ( 'NONE',  ( 0.000000000000000000, 0.8865213383407039016, -1.535500000000022958 ) ) ;
#9471=EDGE_CURVE ( 'NONE', #5655, #1237, #7712, .T. ) ;
#9473=CIRCLE ( 'NONE', #3532, 1.610000000000000098 ) ;
#9479=EDGE_CURVE ( 'NONE', #2833, #2841, #1294, .T. ) ;
#9492=FACE_OUTER_BOUND ( 'NONE', #940, .T. ) ;
#9505=ADVANCED_FACE ( 'NONE', ( #4660 ), #8533, .F. ) ;
#9515=ORIENTED_EDGE ( 'NONE', *, *, #8953, .F. ) ;
#9518=DIRECTION ( 'NONE',  ( 0.000000000000000000, -1.000000000000000000, 9.714451465470119729E-16 ) ) ;
#9537=CARTESIAN_POINT ( 'NONE',  ( -31.74999999999994316, 0.000000000000000000, 0.000000000000000000 ) ) ;
#9547=ORIENTED_EDGE ( 'NONE', *, *, #1622, .F. ) ;
#9566=ORIENTED_EDGE ( 'NONE', *, *, #8953, .T. ) ;
#9583=AXIS2_PLACEMENT_3D ( 'NONE', #6937, #2036, #9228 ) ;
#9587=CARTESIAN_POINT ( 'NONE',  ( 0.2000000000000057288, 4.286263797015736595E-16, -3.500000000000000000 ) ) ;
#9602=AXIS2_PLACEMENT_3D ( 'NONE', #4083, #6394, #1715 ) ;
#9612=AXIS2_PLACEMENT_3D ( 'NONE', #706, #3016, #853 ) ;
#9620=ORIENTED_EDGE ( 'NONE', *, *, #9121, .F. ) ;
#9628=LINE ( 'NONE', #7959, #8262 ) ;
#9651=ORIENTED_EDGE ( 'NONE', *, *, #7128, .T. ) ;
#9655=LINE ( 'NONE', #129, #8763 ) ;
#9666=VERTEX_POINT ( 'NONE', #579 ) ;
#9668=EDGE_LOOP ( 'NONE', ( #6409, #4753, #4443, #7933 ) ) ;
#9674=LINE ( 'NONE', #7135, #3644 ) ;
#9676=ORIENTED_EDGE ( 'NONE', *, *, #10033, .T. ) ;
#9683=DIRECTION ( 'NONE',  ( 0.000000000000000000, 8.191099868251448390E-34, 1.000000000000000000 ) ) ;
#9692=EDGE_CURVE ( 'NONE', #2970, #5864, #5462, .T. ) ;
#9711=EDGE_CURVE ( 'NONE', #2369, #8072, #3724, .T. ) ;
#9712=FACE_OUTER_BOUND ( 'NONE', #9668, .T. ) ;
#9717=DIRECTION ( 'NONE',  ( 0.000000000000000000, 8.191099868251446680E-34, 1.000000000000000000 ) ) ;
#9723=ADVANCED_FACE ( 'NONE', ( #8484 ), #6142, .F. ) ;
#9724=ORIENTED_EDGE ( 'NONE', *, *, #2412, .T. ) ;
#9743=( GEOMETRIC_REPRESENTATION_CONTEXT ( 3 ) GLOBAL_UNCERTAINTY_ASSIGNED_CONTEXT ( ( #6670 ) ) GLOBAL_UNIT_ASSIGNED_CONTEXT ( ( #7797, #7836, #5458 ) ) REPRESENTATION_CONTEXT ( 'NONE', 'WORKASPACE' ) );
#9760=AXIS2_PLACEMENT_3D ( 'NONE', #4993, #1165, #9902 ) ;
#9767=EDGE_LOOP ( 'NONE', ( #7209, #4652 ) ) ;
#9769=ORIENTED_EDGE ( 'NONE', *, *, #9692, .F. ) ;
#9777=ORIENTED_EDGE ( 'NONE', *, *, #8156, .T. ) ;
#9792=EDGE_CURVE ( 'NONE', #3268, #9145, #3475, .T. ) ;
#9809=PRODUCT_DEFINITION_CONTEXT ( 'detailed design', #6045, 'design' ) ;
#9817=VERTEX_POINT ( 'NONE', #5426 ) ;
#9828=CARTESIAN_POINT ( 'NONE',  ( 4.000000000000003553, 4.286263797015736595E-16, -3.500000000000000000 ) ) ;
#9856=VECTOR ( 'NONE', #8814, 1000.000000000000000 ) ;
#9883=PRODUCT ( 'socket head cap screw_iso_ISO 4762 M4 x 10 - 10N', 'socket head cap screw_iso_ISO 4762 M4 x 10 - 10N', '', ( #4385 ) ) ;
#9888=CARTESIAN_POINT ( 'NONE',  ( 4.000000000000007105, -1.802041971015319193E-33, -2.200000000000001066 ) ) ;
#9902=DIRECTION ( 'NONE',  ( 0.000000000000000000, -8.191099868251446680E-34, -1.000000000000000000 ) ) ;
#9909=ADVANCED_FACE ( 'NONE', ( #1293 ), #4303, .T. ) ;
#9927=AXIS2_PLACEMENT_3D ( 'NONE', #4196, #8325, #7345 ) ;
#9929=EDGE_LOOP ( 'NONE', ( #5691, #1368, #7918, #4178 ) ) ;
#9933=EDGE_CURVE ( 'NONE', #6635, #3268, #9674, .T. ) ;
#9941=VECTOR ( 'NONE', #7517, 1000.000000000000000 ) ;
#9956=VECTOR ( 'NONE', #8478, 1000.000000000000000 ) ;
#9957=FACE_OUTER_BOUND ( 'NONE', #3759, .T. ) ;
#9968=CARTESIAN_POINT ( 'NONE',  ( 2.000000000000001776, 1.773042676681366281, 0.000000000000000000 ) ) ;
#9990=CARTESIAN_POINT ( 'NONE',  ( 4.000000000000003553, 0.000000000000000000, 0.000000000000000000 ) ) ;
#10025=EDGE_LOOP ( 'NONE', ( #4520, #204, #8813 ) ) ;
#10033=EDGE_CURVE ( 'NONE', #5107, #1541, #9628, .T. ) ;
#10055=ADVANCED_FACE ( 'NONE', ( #5529 ), #3209, .F. ) ;
#10104=CARTESIAN_POINT ( 'NONE',  ( 2.000000000000001776, 1.387778780781445676E-14, -1.535500000000022958 ) ) ;
#10108=DIRECTION ( 'NONE',  ( 0.000000000000000000, -0.8660254037844391517, -0.4999999999999992228 ) ) ;
#10134=CARTESIAN_POINT ( 'NONE',  ( 2.000000000000001776, 1.773042676681366281, 0.000000000000000000 ) ) ;
#10152=LINE ( 'NONE', #3065, #695 ) ;
#10183=CARTESIAN_POINT ( 'NONE',  ( 0.000000000000000000, 0.000000000000000000, 0.000000000000000000 ) ) ;
#10197=DIRECTION ( 'NONE',  ( 0.000000000000000000, 8.191099868251448390E-34, 1.000000000000000000 ) ) ;
#10200=ORIENTED_EDGE ( 'NONE', *, *, #5587, .F. ) ;
#10202=CYLINDRICAL_SURFACE ( 'NONE', #4240, 3.500000000000000000 ) ;
#10204=CARTESIAN_POINT ( 'NONE',  ( 2.000000000000001776, 1.773042676681366281, 0.000000000000000000 ) ) ;
#10223=ADVANCED_FACE ( 'NONE', ( #1898 ), #1842, .F. ) ;
ENDSEC;
END-ISO-10303-21;
